ISO-10303-21;
HEADER;
/* Generated by software containing ST-Developer
 * from STEP Tools, Inc. (www.steptools.com) 
 */

FILE_DESCRIPTION(
/* description */ ('Belt conveyor head drive unit'),
/* implementation_level */ '2;1');

FILE_NAME(
/* name */ 'Output M3 set screw.step',
/* time_stamp */ '2026-10-28T03:26:19-07:00',
/* author */ (''),
/* organization */ (''),
/* preprocessor_version */ 'ST-DEVELOPER v20.2',
/* originating_system */ 'Autodesk Translation Framework v15.17.0.0',
/* authorisation */ '');

FILE_SCHEMA (('AUTOMOTIVE_DESIGN { 1 0 10303 214 3 1 1 }'));
ENDSEC;

DATA;
#10=MECHANICAL_DESIGN_GEOMETRIC_PRESENTATION_REPRESENTATION('',(#919),#27069);
#765=SHAPE_REPRESENTATION_RELATIONSHIP('SRR','None',#27414,#834);
#834=ADVANCED_BREP_SHAPE_REPRESENTATION('',(#1000),#27056);
#919=STYLED_ITEM('',(#27804),#1000);
#1000=MANIFOLD_SOLID_BREP('Body1',#13788);
#1580=PLANE('',#15912);
#1581=PLANE('',#15913);
#2261=FACE_OUTER_BOUND('',#3289,.T.);
#2262=FACE_OUTER_BOUND('',#3290,.T.);
#2263=FACE_OUTER_BOUND('',#3291,.T.);
#3289=EDGE_LOOP('',(#11670,#11671,#11672,#11673));
#3290=EDGE_LOOP('',(#11674));
#3291=EDGE_LOOP('',(#11675));
#4125=LINE('',#25384,#4917);
#4917=VECTOR('',#19759,0.15);
#5725=CIRCLE('',#15910,0.15);
#5726=CIRCLE('',#15911,0.15);
#6881=VERTEX_POINT('',#25381);
#6882=VERTEX_POINT('',#25383);
#8527=EDGE_CURVE('',#6881,#6881,#5725,.T.);
#8528=EDGE_CURVE('',#6881,#6882,#4125,.T.);
#8529=EDGE_CURVE('',#6882,#6882,#5726,.T.);
#11670=ORIENTED_EDGE('',*,*,#8527,.F.);
#11671=ORIENTED_EDGE('',*,*,#8528,.T.);
#11672=ORIENTED_EDGE('',*,*,#8529,.T.);
#11673=ORIENTED_EDGE('',*,*,#8528,.F.);
#11674=ORIENTED_EDGE('',*,*,#8527,.T.);
#11675=ORIENTED_EDGE('',*,*,#8529,.F.);
#12799=CYLINDRICAL_SURFACE('',#15909,0.15);
#13540=ADVANCED_FACE('',(#2261),#12799,.T.);
#13541=ADVANCED_FACE('',(#2262),#1580,.T.);
#13542=ADVANCED_FACE('',(#2263),#1581,.F.);
#13788=CLOSED_SHELL('',(#13540,#13541,#13542));
#15908=AXIS2_PLACEMENT_3D('',#25379,#19753,#19754);
#15909=AXIS2_PLACEMENT_3D('',#25380,#19755,#19756);
#15910=AXIS2_PLACEMENT_3D('',#25382,#19757,#19758);
#15911=AXIS2_PLACEMENT_3D('',#25385,#19760,#19761);
#15912=AXIS2_PLACEMENT_3D('',#25386,#19762,#19763);
#15913=AXIS2_PLACEMENT_3D('',#25387,#19764,#19765);
#19753=DIRECTION('axis',(0.,0.,1.));
#19754=DIRECTION('refdir',(1.,0.,0.));
#19755=DIRECTION('center_axis',(0.,0.,1.));
#19756=DIRECTION('ref_axis',(1.,0.,0.));
#19757=DIRECTION('center_axis',(0.,0.,1.));
#19758=DIRECTION('ref_axis',(1.,0.,0.));
#19759=DIRECTION('',(0.,0.,-1.));
#19760=DIRECTION('center_axis',(0.,0.,1.));
#19761=DIRECTION('ref_axis',(1.,0.,0.));
#19762=DIRECTION('center_axis',(0.,0.,1.));
#19763=DIRECTION('ref_axis',(1.,0.,0.));
#19764=DIRECTION('center_axis',(0.,0.,1.));
#19765=DIRECTION('ref_axis',(1.,0.,0.));
#25379=CARTESIAN_POINT('',(0.,0.,0.));
#25380=CARTESIAN_POINT('Origin',(6.97091003018116,-4.,6.));
#25381=CARTESIAN_POINT('',(6.82091003018116,-4.,6.4));
#25382=CARTESIAN_POINT('Origin',(6.97091003018116,-4.,6.4));
#25383=CARTESIAN_POINT('',(6.82091003018116,-4.,6.));
#25384=CARTESIAN_POINT('',(6.82091003018116,-4.,6.));
#25385=CARTESIAN_POINT('Origin',(6.97091003018116,-4.,6.));
#25386=CARTESIAN_POINT('Origin',(6.97091003018116,-4.,6.4));
#25387=CARTESIAN_POINT('Origin',(6.97091003018116,-4.,6.));
#26979=UNCERTAINTY_MEASURE_WITH_UNIT(LENGTH_MEASURE(0.001),#27070,
'DISTANCE_ACCURACY_VALUE',
'Maximum model space distance between geometric entities at asserted c
onnectivities');
#26992=UNCERTAINTY_MEASURE_WITH_UNIT(LENGTH_MEASURE(0.001),#27070,
'DISTANCE_ACCURACY_VALUE',
'Maximum model space distance between geometric entities at asserted c
onnectivities');
#27056=(
GEOMETRIC_REPRESENTATION_CONTEXT(3)
GLOBAL_UNCERTAINTY_ASSIGNED_CONTEXT((#26979))
GLOBAL_UNIT_ASSIGNED_CONTEXT((#27070,#27072,#27073))
REPRESENTATION_CONTEXT('','3D')
);
#27069=(
GEOMETRIC_REPRESENTATION_CONTEXT(3)
GLOBAL_UNCERTAINTY_ASSIGNED_CONTEXT((#26992))
GLOBAL_UNIT_ASSIGNED_CONTEXT((#27070,#27072,#27073))
REPRESENTATION_CONTEXT('','3D')
);
#27070=(
LENGTH_UNIT()
NAMED_UNIT(*)
SI_UNIT(.CENTI.,.METRE.)
);
#27072=(
NAMED_UNIT(*)
PLANE_ANGLE_UNIT()
SI_UNIT($,.RADIAN.)
);
#27073=(
NAMED_UNIT(*)
SI_UNIT($,.STERADIAN.)
SOLID_ANGLE_UNIT()
);
#27137=SHAPE_DEFINITION_REPRESENTATION(#27225,#27414);
#27225=PRODUCT_DEFINITION_SHAPE('',$,#27491);
#27414=SHAPE_REPRESENTATION('',(#15908),#27056);
#27427=PRODUCT_DEFINITION_CONTEXT('part definition',#27657,'design');
#27491=PRODUCT_DEFINITION('Output M3 set screw','Output M3 set screw',#27567,
#27427);
#27567=PRODUCT_DEFINITION_FORMATION('',$,#27722);
#27657=APPLICATION_CONTEXT(
'Core Data for Automotive Mechanical Design Process');
#27658=PRODUCT_CONTEXT('part definition',#27657,'mechanical');
#27722=PRODUCT('Output M3 set screw','Output M3 set screw',
'Output M3 set screw',(#27658));
#27798=COLOUR_RGB('Black',0.12,0.14,0.17);
#27799=FILL_AREA_STYLE_COLOUR('',#27798);
#27800=FILL_AREA_STYLE('',(#27799));
#27801=SURFACE_STYLE_FILL_AREA(#27800);
#27802=SURFACE_SIDE_STYLE('',(#27801));
#27803=SURFACE_STYLE_USAGE(.BOTH.,#27802);
#27804=PRESENTATION_STYLE_ASSIGNMENT((#27803));
ENDSEC;
END-ISO-10303-21;
